ISO-10303-21;
HEADER;
/* Generated by software containing ST-Developer
 * from STEP Tools, Inc. (www.steptools.com) 
 */

FILE_DESCRIPTION(
/* description */ ('Cam-driven reciprocating slide'),
/* implementation_level */ '2;1');

FILE_NAME(
/* name */ 'Inner race sleeve 15 mm (1).step',
/* time_stamp */ '2026-10-28T03:25:20-07:00',
/* author */ (''),
/* organization */ (''),
/* preprocessor_version */ 'ST-DEVELOPER v20.2',
/* originating_system */ 'Autodesk Translation Framework v15.17.0.0',
/* authorisation */ '');

FILE_SCHEMA (('AUTOMOTIVE_DESIGN { 1 0 10303 214 3 1 1 }'));
ENDSEC;

DATA;
#10=MECHANICAL_DESIGN_GEOMETRIC_PRESENTATION_REPRESENTATION('',(#455),#13277);
#374=SHAPE_REPRESENTATION_RELATIONSHIP('SRR','None',#13470,#411);
#411=ADVANCED_BREP_SHAPE_REPRESENTATION('',(#497),#13265);
#455=STYLED_ITEM('',(#13720),#497);
#497=MANIFOLD_SOLID_BREP('Body1',#6433);
#650=FACE_BOUND('',#1712,.T.);
#651=FACE_BOUND('',#1714,.T.);
#839=PLANE('',#7447);
#840=PLANE('',#7448);
#1187=FACE_OUTER_BOUND('',#1709,.T.);
#1188=FACE_OUTER_BOUND('',#1710,.T.);
#1189=FACE_OUTER_BOUND('',#1711,.T.);
#1190=FACE_OUTER_BOUND('',#1713,.T.);
#1709=EDGE_LOOP('',(#5528,#5529,#5530,#5531));
#1710=EDGE_LOOP('',(#5532,#5533,#5534,#5535));
#1711=EDGE_LOOP('',(#5536));
#1712=EDGE_LOOP('',(#5537));
#1713=EDGE_LOOP('',(#5538));
#1714=EDGE_LOOP('',(#5539));
#2150=LINE('',#12724,#2589);
#2151=LINE('',#12730,#2590);
#2589=VECTOR('',#9166,0.605);
#2590=VECTOR('',#9173,0.8);
#2975=CIRCLE('',#7442,0.605);
#2976=CIRCLE('',#7443,0.605);
#2977=CIRCLE('',#7445,0.8);
#2978=CIRCLE('',#7446,0.8);
#3438=VERTEX_POINT('',#12721);
#3439=VERTEX_POINT('',#12723);
#3440=VERTEX_POINT('',#12727);
#3441=VERTEX_POINT('',#12729);
#4154=EDGE_CURVE('',#3438,#3438,#2975,.T.);
#4155=EDGE_CURVE('',#3438,#3439,#2150,.T.);
#4156=EDGE_CURVE('',#3439,#3439,#2976,.T.);
#4157=EDGE_CURVE('',#3440,#3440,#2977,.T.);
#4158=EDGE_CURVE('',#3440,#3441,#2151,.T.);
#4159=EDGE_CURVE('',#3441,#3441,#2978,.T.);
#5528=ORIENTED_EDGE('',*,*,#4154,.F.);
#5529=ORIENTED_EDGE('',*,*,#4155,.T.);
#5530=ORIENTED_EDGE('',*,*,#4156,.T.);
#5531=ORIENTED_EDGE('',*,*,#4155,.F.);
#5532=ORIENTED_EDGE('',*,*,#4157,.F.);
#5533=ORIENTED_EDGE('',*,*,#4158,.T.);
#5534=ORIENTED_EDGE('',*,*,#4159,.T.);
#5535=ORIENTED_EDGE('',*,*,#4158,.F.);
#5536=ORIENTED_EDGE('',*,*,#4157,.T.);
#5537=ORIENTED_EDGE('',*,*,#4154,.T.);
#5538=ORIENTED_EDGE('',*,*,#4159,.F.);
#5539=ORIENTED_EDGE('',*,*,#4156,.F.);
#5992=CYLINDRICAL_SURFACE('',#7441,0.605);
#5993=CYLINDRICAL_SURFACE('',#7444,0.8);
#6305=ADVANCED_FACE('',(#1187),#5992,.F.);
#6306=ADVANCED_FACE('',(#1188),#5993,.T.);
#6307=ADVANCED_FACE('',(#1189,#650),#839,.T.);
#6308=ADVANCED_FACE('',(#1190,#651),#840,.F.);
#6433=CLOSED_SHELL('',(#6305,#6306,#6307,#6308));
#7440=AXIS2_PLACEMENT_3D('',#12719,#9160,#9161);
#7441=AXIS2_PLACEMENT_3D('',#12720,#9162,#9163);
#7442=AXIS2_PLACEMENT_3D('',#12722,#9164,#9165);
#7443=AXIS2_PLACEMENT_3D('',#12725,#9167,#9168);
#7444=AXIS2_PLACEMENT_3D('',#12726,#9169,#9170);
#7445=AXIS2_PLACEMENT_3D('',#12728,#9171,#9172);
#7446=AXIS2_PLACEMENT_3D('',#12731,#9174,#9175);
#7447=AXIS2_PLACEMENT_3D('',#12732,#9176,#9177);
#7448=AXIS2_PLACEMENT_3D('',#12733,#9178,#9179);
#9160=DIRECTION('axis',(0.,0.,1.));
#9161=DIRECTION('refdir',(1.,0.,0.));
#9162=DIRECTION('center_axis',(0.,1.,0.));
#9163=DIRECTION('ref_axis',(1.,0.,0.));
#9164=DIRECTION('center_axis',(0.,-1.,0.));
#9165=DIRECTION('ref_axis',(1.,0.,0.));
#9166=DIRECTION('',(0.,-1.,0.));
#9167=DIRECTION('center_axis',(0.,-1.,0.));
#9168=DIRECTION('ref_axis',(1.,0.,0.));
#9169=DIRECTION('center_axis',(0.,1.,0.));
#9170=DIRECTION('ref_axis',(1.,0.,0.));
#9171=DIRECTION('center_axis',(0.,1.,0.));
#9172=DIRECTION('ref_axis',(1.,0.,0.));
#9173=DIRECTION('',(0.,-1.,0.));
#9174=DIRECTION('center_axis',(0.,1.,0.));
#9175=DIRECTION('ref_axis',(1.,0.,0.));
#9176=DIRECTION('center_axis',(0.,1.,0.));
#9177=DIRECTION('ref_axis',(1.,0.,0.));
#9178=DIRECTION('center_axis',(0.,1.,0.));
#9179=DIRECTION('ref_axis',(1.,0.,0.));
#12719=CARTESIAN_POINT('',(0.,0.,0.));
#12720=CARTESIAN_POINT('Origin',(0.,3.,4.));
#12721=CARTESIAN_POINT('',(-0.605,4.5,4.));
#12722=CARTESIAN_POINT('Origin',(0.,4.5,4.));
#12723=CARTESIAN_POINT('',(-0.605,3.,4.));
#12724=CARTESIAN_POINT('',(-0.605,3.,4.));
#12725=CARTESIAN_POINT('Origin',(0.,3.,4.));
#12726=CARTESIAN_POINT('Origin',(0.,3.,4.));
#12727=CARTESIAN_POINT('',(-0.8,4.5,4.));
#12728=CARTESIAN_POINT('Origin',(0.,4.5,4.));
#12729=CARTESIAN_POINT('',(-0.8,3.,4.));
#12730=CARTESIAN_POINT('',(-0.8,3.,4.));
#12731=CARTESIAN_POINT('Origin',(0.,3.,4.));
#12732=CARTESIAN_POINT('Origin',(0.,4.5,4.));
#12733=CARTESIAN_POINT('Origin',(0.,3.,4.));
#13221=UNCERTAINTY_MEASURE_WITH_UNIT(LENGTH_MEASURE(0.001),#13278,
'DISTANCE_ACCURACY_VALUE',
'Maximum model space distance between geometric entities at asserted c
onnectivities');
#13233=UNCERTAINTY_MEASURE_WITH_UNIT(LENGTH_MEASURE(0.001),#13278,
'DISTANCE_ACCURACY_VALUE',
'Maximum model space distance between geometric entities at asserted c
onnectivities');
#13265=(
GEOMETRIC_REPRESENTATION_CONTEXT(3)
GLOBAL_UNCERTAINTY_ASSIGNED_CONTEXT((#13221))
GLOBAL_UNIT_ASSIGNED_CONTEXT((#13278,#13280,#13281))
REPRESENTATION_CONTEXT('','3D')
);
#13277=(
GEOMETRIC_REPRESENTATION_CONTEXT(3)
GLOBAL_UNCERTAINTY_ASSIGNED_CONTEXT((#13233))
GLOBAL_UNIT_ASSIGNED_CONTEXT((#13278,#13280,#13281))
REPRESENTATION_CONTEXT('','3D')
);
#13278=(
LENGTH_UNIT()
NAMED_UNIT(*)
SI_UNIT(.CENTI.,.METRE.)
);
#13280=(
NAMED_UNIT(*)
PLANE_ANGLE_UNIT()
SI_UNIT($,.RADIAN.)
);
#13281=(
NAMED_UNIT(*)
SI_UNIT($,.STERADIAN.)
SOLID_ANGLE_UNIT()
);
#13313=SHAPE_DEFINITION_REPRESENTATION(#13363,#13470);
#13363=PRODUCT_DEFINITION_SHAPE('',$,#13514);
#13470=SHAPE_REPRESENTATION('',(#7440),#13265);
#13482=PRODUCT_DEFINITION_CONTEXT('part definition',#13613,'design');
#13514=PRODUCT_DEFINITION('Inner race sleeve 15 mm (1)',
'Inner race sleeve 15 mm (1)',#13557,#13482);
#13557=PRODUCT_DEFINITION_FORMATION('',$,#13646);
#13613=APPLICATION_CONTEXT(
'Core Data for Automotive Mechanical Design Process');
#13614=PRODUCT_CONTEXT('part definition',#13613,'mechanical');
#13646=PRODUCT('Inner race sleeve 15 mm (1)',
'Inner race sleeve 15 mm (1)','Inner race sleeve 15 mm (1)',(#13614));
#13714=COLOUR_RGB('Grey',0.48,0.52,0.57);
#13715=FILL_AREA_STYLE_COLOUR('',#13714);
#13716=FILL_AREA_STYLE('',(#13715));
#13717=SURFACE_STYLE_FILL_AREA(#13716);
#13718=SURFACE_SIDE_STYLE('',(#13717));
#13719=SURFACE_STYLE_USAGE(.BOTH.,#13718);
#13720=PRESENTATION_STYLE_ASSIGNMENT((#13719));
ENDSEC;
END-ISO-10303-21;
